ISO-10303-21;
HEADER;
FILE_DESCRIPTION((''),'2;1');
FILE_NAME('SPRING_HOOK_PIN.step','2026-10-01T22:06:14-07:00',(''),(''),'','','');
FILE_SCHEMA (('AUTOMOTIVE_DESIGN { 1 0 10303 214 3 1 1 }'));
ENDSEC;
DATA;
#10=MECHANICAL_DESIGN_GEOMETRIC_PRESENTATION_REPRESENTATION('',(#1034),#50440);
#933=SHAPE_REPRESENTATION_RELATIONSHIP('SRR','None',#50668,#978) ;
#978=ADVANCED_BREP_SHAPE_REPRESENTATION('',(#1087),#50437) ;
#1034=STYLED_ITEM('',(#50883),#1087) ;
#1087=MANIFOLD_SOLID_BREP('SPRING_HOOK_PIN',#28712) ;
#1406=FACE_BOUND('',#5706,.T.) ;
#2331=PLANE('',#32258) ;
#2332=PLANE('',#32263) ;
#2333=PLANE('',#32266) ;
#3857=FACE_OUTER_BOUND('',#5705,.T.) ;
#3858=FACE_OUTER_BOUND('',#5707,.T.) ;
#3859=FACE_OUTER_BOUND('',#5708,.T.) ;
#3860=FACE_OUTER_BOUND('',#5709,.T.) ;
#3861=FACE_OUTER_BOUND('',#5710,.T.) ;
#5705=EDGE_LOOP('',(#26475)) ;
#5706=EDGE_LOOP('',(#26476)) ;
#5707=EDGE_LOOP('',(#26477,#26478,#26479,#26480)) ;
#5708=EDGE_LOOP('',(#26481)) ;
#5709=EDGE_LOOP('',(#26482,#26483,#26484,#26485)) ;
#5710=EDGE_LOOP('',(#26486)) ;
#8199=LINE('',#50090,#10671) ;
#8200=LINE('',#50094,#10672) ;
#10671=VECTOR('',#40950,0.45) ;
#10672=VECTOR('',#40955,0.245) ;
#11810=CIRCLE('',#32259,0.45) ;
#11811=CIRCLE('',#32260,0.245) ;
#11812=CIRCLE('',#32262,0.45) ;
#11813=CIRCLE('',#32265,0.245) ;
#14504=VERTEX_POINT('',#50083) ;
#14505=VERTEX_POINT('',#50085) ;
#14506=VERTEX_POINT('',#50088) ;
#14507=VERTEX_POINT('',#50093) ;
#18503=EDGE_CURVE('',#14504,#14504,#11810,.T.) ;
#18504=EDGE_CURVE('',#14505,#14505,#11811,.T.) ;
#18505=EDGE_CURVE('',#14506,#14506,#11812,.T.) ;
#18506=EDGE_CURVE('',#14506,#14504,#8199,.T.) ;
#18507=EDGE_CURVE('',#14505,#14507,#8200,.T.) ;
#18508=EDGE_CURVE('',#14507,#14507,#11813,.T.) ;
#26475=ORIENTED_EDGE('',*,*,#18503,.T.) ;
#26476=ORIENTED_EDGE('',*,*,#18504,.T.) ;
#26477=ORIENTED_EDGE('',*,*,#18505,.F.) ;
#26478=ORIENTED_EDGE('',*,*,#18506,.T.) ;
#26479=ORIENTED_EDGE('',*,*,#18503,.F.) ;
#26480=ORIENTED_EDGE('',*,*,#18506,.F.) ;
#26481=ORIENTED_EDGE('',*,*,#18505,.T.) ;
#26482=ORIENTED_EDGE('',*,*,#18504,.F.) ;
#26483=ORIENTED_EDGE('',*,*,#18507,.T.) ;
#26484=ORIENTED_EDGE('',*,*,#18508,.F.) ;
#26485=ORIENTED_EDGE('',*,*,#18507,.F.) ;
#26486=ORIENTED_EDGE('',*,*,#18508,.T.) ;
#27058=CYLINDRICAL_SURFACE('',#32261,0.45) ;
#27059=CYLINDRICAL_SURFACE('',#32264,0.245) ;
#28592=ADVANCED_FACE('',(#3857,#1406),#2331,.T.) ;
#28593=ADVANCED_FACE('',(#3858),#27058,.T.) ;
#28594=ADVANCED_FACE('',(#3859),#2332,.T.) ;
#28595=ADVANCED_FACE('',(#3860),#27059,.T.) ;
#28596=ADVANCED_FACE('',(#3861),#2333,.T.) ;
#28712=CLOSED_SHELL('',(#28592,#28593,#28594,#28595,#28596)) ;
#32257=AXIS2_PLACEMENT_3D('',#50081,#40938,#40939) ;
#32258=AXIS2_PLACEMENT_3D('',#50082,#40940,#40941) ;
#32259=AXIS2_PLACEMENT_3D('',#50084,#40942,#40943) ;
#32260=AXIS2_PLACEMENT_3D('',#50086,#40944,#40945) ;
#32261=AXIS2_PLACEMENT_3D('',#50087,#40946,#40947) ;
#32262=AXIS2_PLACEMENT_3D('',#50089,#40948,#40949) ;
#32263=AXIS2_PLACEMENT_3D('',#50091,#40951,#40952) ;
#32264=AXIS2_PLACEMENT_3D('',#50092,#40953,#40954) ;
#32265=AXIS2_PLACEMENT_3D('',#50095,#40956,#40957) ;
#32266=AXIS2_PLACEMENT_3D('',#50096,#40958,#40959) ;
#40938=DIRECTION('axis',(0.,0.,1.)) ;
#40939=DIRECTION('refdir',(1.,0.,0.)) ;
#40940=DIRECTION('center_axis',(0.,0.,-1.)) ;
#40941=DIRECTION('ref_axis',(-1.,0.,0.)) ;
#40942=DIRECTION('center_axis',(0.,0.,-1.)) ;
#40943=DIRECTION('ref_axis',(1.,0.,0.)) ;
#40944=DIRECTION('center_axis',(0.,0.,1.)) ;
#40945=DIRECTION('ref_axis',(1.,0.,0.)) ;
#40946=DIRECTION('center_axis',(0.,0.,1.)) ;
#40947=DIRECTION('ref_axis',(1.,0.,0.)) ;
#40948=DIRECTION('center_axis',(0.,0.,1.)) ;
#40949=DIRECTION('ref_axis',(1.,0.,0.)) ;
#40950=DIRECTION('',(0.,0.,-1.)) ;
#40951=DIRECTION('center_axis',(0.,0.,1.)) ;
#40952=DIRECTION('ref_axis',(1.,0.,0.)) ;
#40953=DIRECTION('center_axis',(0.,0.,1.)) ;
#40954=DIRECTION('ref_axis',(1.,0.,0.)) ;
#40955=DIRECTION('',(0.,0.,-1.)) ;
#40956=DIRECTION('center_axis',(0.,0.,-1.)) ;
#40957=DIRECTION('ref_axis',(1.,0.,0.)) ;
#40958=DIRECTION('center_axis',(0.,0.,-1.)) ;
#40959=DIRECTION('ref_axis',(-1.,0.,0.)) ;
#50081=CARTESIAN_POINT('',(0.,0.,0.)) ;
#50082=CARTESIAN_POINT('Origin',(0.,0.,44.)) ;
#50083=CARTESIAN_POINT('',(-0.45,-5.51091059616309E-17,44.)) ;
#50084=CARTESIAN_POINT('Origin',(0.,0.,44.)) ;
#50085=CARTESIAN_POINT('',(-0.245,-3.00038465791102E-17,44.)) ;
#50086=CARTESIAN_POINT('Origin',(0.,0.,44.)) ;
#50087=CARTESIAN_POINT('Origin',(0.,0.,44.1)) ;
#50088=CARTESIAN_POINT('',(-0.45,-5.51091059616309E-17,44.2)) ;
#50089=CARTESIAN_POINT('Origin',(0.,0.,44.2)) ;
#50090=CARTESIAN_POINT('',(-0.45,-5.51091059616309E-17,44.1)) ;
#50091=CARTESIAN_POINT('Origin',(0.,0.,44.2)) ;
#50092=CARTESIAN_POINT('Origin',(0.,0.,43.2)) ;
#50093=CARTESIAN_POINT('',(-0.245,-3.00038465791102E-17,42.4)) ;
#50094=CARTESIAN_POINT('',(-0.245,-3.00038465791102E-17,43.2)) ;
#50095=CARTESIAN_POINT('Origin',(0.,0.,42.4)) ;
#50096=CARTESIAN_POINT('Origin',(0.,0.,42.4)) ;
#50384=UNCERTAINTY_MEASURE_WITH_UNIT(LENGTH_MEASURE(0.001),#50441,
'DISTANCE_ACCURACY_VALUE',
'Maximum model space distance between geometric entities at asserted c
onnectivities') ;
#50387=UNCERTAINTY_MEASURE_WITH_UNIT(LENGTH_MEASURE(0.001),#50441,
'DISTANCE_ACCURACY_VALUE',
'Maximum model space distance between geometric entities at asserted c
onnectivities') ;
#50437=(
GEOMETRIC_REPRESENTATION_CONTEXT(3)
GLOBAL_UNCERTAINTY_ASSIGNED_CONTEXT((#50384))
GLOBAL_UNIT_ASSIGNED_CONTEXT((#50441,#50443,#50444))
REPRESENTATION_CONTEXT('','3D')
) ;
#50440=(
GEOMETRIC_REPRESENTATION_CONTEXT(3)
GLOBAL_UNCERTAINTY_ASSIGNED_CONTEXT((#50387))
GLOBAL_UNIT_ASSIGNED_CONTEXT((#50441,#50443,#50444))
REPRESENTATION_CONTEXT('','3D')
) ;
#50441=(
LENGTH_UNIT()
NAMED_UNIT(*)
SI_UNIT(.CENTI.,.METRE.)
) ;
#50443=(
NAMED_UNIT(*)
PLANE_ANGLE_UNIT()
SI_UNIT($,.RADIAN.)
) ;
#50444=(
NAMED_UNIT(*)
SI_UNIT($,.STERADIAN.)
SOLID_ANGLE_UNIT()
) ;
#50494=SHAPE_DEFINITION_REPRESENTATION(#50590,#50668) ;
#50590=PRODUCT_DEFINITION_SHAPE('',$,#50721) ;
#50668=SHAPE_REPRESENTATION('',(#32257),#50437) ;
#50671=PRODUCT_DEFINITION_CONTEXT('part definition',#50829,'design') ;
#50721=PRODUCT_DEFINITION('SPRING_HOOK_PIN','SPRING_HOOK_PIN',#50773,
#50671) ;
#50773=PRODUCT_DEFINITION_FORMATION('',$,#50880) ;
#50829=APPLICATION_CONTEXT(
'Core Data for Automotive Mechanical Design Process') ;
#50830=PRODUCT_CONTEXT('part definition',#50829,'mechanical') ;
#50880=PRODUCT('SPRING_HOOK_PIN','SPRING_HOOK_PIN',$,(#50830)) ;
#50883=PRESENTATION_STYLE_ASSIGNMENT((#50890)) ;
#50890=SURFACE_STYLE_USAGE(.BOTH.,#50897) ;
#50897=SURFACE_SIDE_STYLE('',(#50904)) ;
#50904=SURFACE_STYLE_FILL_AREA(#50911) ;
#50911=FILL_AREA_STYLE('Steel - Satin',(#50918)) ;
#50918=FILL_AREA_STYLE_COLOUR('Steel - Satin',#50925) ;
#50925=COLOUR_RGB('Steel - Satin', 0.31764706, 0.68627451, 0.89019608) ;
ENDSEC;
END-ISO-10303-21;
